ISO-10303-21;
HEADER;
/* Generated by software containing ST-Developer
 * from STEP Tools, Inc. (www.steptools.com) 
 */

FILE_DESCRIPTION(
/* description */ ('PAT-091'),
/* implementation_level */ '2;1');

FILE_NAME(
/* name */ 'Axle distance sleeve 10 mm (2).step',
/* time_stamp */ '2026-10-27T15:34:44-07:00',
/* author */ (''),
/* organization */ (''),
/* preprocessor_version */ 'ST-DEVELOPER v20.2',
/* originating_system */ 'Autodesk Translation Framework v15.17.0.0',
/* authorisation */ '');

FILE_SCHEMA (('AUTOMOTIVE_DESIGN { 1 0 10303 214 3 1 1 }'));
ENDSEC;

DATA;
#10=MECHANICAL_DESIGN_GEOMETRIC_PRESENTATION_REPRESENTATION('',(#1041),#25100);
#821=SHAPE_REPRESENTATION_RELATIONSHIP('SRR','None',#25587,#931);
#931=ADVANCED_BREP_SHAPE_REPRESENTATION('',(#1163),#25057);
#1041=STYLED_ITEM('',(#26191),#1163);
#1163=MANIFOLD_SOLID_BREP('Body1',#13320);
#1520=FACE_BOUND('',#3714,.T.);
#1521=FACE_BOUND('',#3716,.T.);
#1933=PLANE('',#15662);
#1934=PLANE('',#15663);
#2588=FACE_OUTER_BOUND('',#3711,.T.);
#2589=FACE_OUTER_BOUND('',#3712,.T.);
#2590=FACE_OUTER_BOUND('',#3713,.T.);
#2591=FACE_OUTER_BOUND('',#3715,.T.);
#3711=EDGE_LOOP('',(#11056,#11057,#11058,#11059));
#3712=EDGE_LOOP('',(#11060,#11061,#11062,#11063));
#3713=EDGE_LOOP('',(#11064));
#3714=EDGE_LOOP('',(#11065));
#3715=EDGE_LOOP('',(#11066));
#3716=EDGE_LOOP('',(#11067));
#4696=LINE('',#23369,#5436);
#4697=LINE('',#23375,#5437);
#5436=VECTOR('',#19186,0.605);
#5437=VECTOR('',#19193,0.800000000000001);
#6070=CIRCLE('',#15657,0.605);
#6071=CIRCLE('',#15658,0.605);
#6072=CIRCLE('',#15660,0.800000000000001);
#6073=CIRCLE('',#15661,0.800000000000001);
#7075=VERTEX_POINT('',#23366);
#7076=VERTEX_POINT('',#23368);
#7077=VERTEX_POINT('',#23372);
#7078=VERTEX_POINT('',#23374);
#8463=EDGE_CURVE('',#7075,#7075,#6070,.T.);
#8464=EDGE_CURVE('',#7075,#7076,#4696,.T.);
#8465=EDGE_CURVE('',#7076,#7076,#6071,.T.);
#8466=EDGE_CURVE('',#7077,#7077,#6072,.T.);
#8467=EDGE_CURVE('',#7077,#7078,#4697,.T.);
#8468=EDGE_CURVE('',#7078,#7078,#6073,.T.);
#11056=ORIENTED_EDGE('',*,*,#8463,.F.);
#11057=ORIENTED_EDGE('',*,*,#8464,.T.);
#11058=ORIENTED_EDGE('',*,*,#8465,.T.);
#11059=ORIENTED_EDGE('',*,*,#8464,.F.);
#11060=ORIENTED_EDGE('',*,*,#8466,.F.);
#11061=ORIENTED_EDGE('',*,*,#8467,.T.);
#11062=ORIENTED_EDGE('',*,*,#8468,.T.);
#11063=ORIENTED_EDGE('',*,*,#8467,.F.);
#11064=ORIENTED_EDGE('',*,*,#8466,.T.);
#11065=ORIENTED_EDGE('',*,*,#8463,.T.);
#11066=ORIENTED_EDGE('',*,*,#8468,.F.);
#11067=ORIENTED_EDGE('',*,*,#8465,.F.);
#12298=CYLINDRICAL_SURFACE('',#15656,0.605);
#12299=CYLINDRICAL_SURFACE('',#15659,0.800000000000001);
#12955=ADVANCED_FACE('',(#2588),#12298,.F.);
#12956=ADVANCED_FACE('',(#2589),#12299,.T.);
#12957=ADVANCED_FACE('',(#2590,#1520),#1933,.T.);
#12958=ADVANCED_FACE('',(#2591,#1521),#1934,.F.);
#13320=CLOSED_SHELL('',(#12955,#12956,#12957,#12958));
#15655=AXIS2_PLACEMENT_3D('',#23364,#19180,#19181);
#15656=AXIS2_PLACEMENT_3D('',#23365,#19182,#19183);
#15657=AXIS2_PLACEMENT_3D('',#23367,#19184,#19185);
#15658=AXIS2_PLACEMENT_3D('',#23370,#19187,#19188);
#15659=AXIS2_PLACEMENT_3D('',#23371,#19189,#19190);
#15660=AXIS2_PLACEMENT_3D('',#23373,#19191,#19192);
#15661=AXIS2_PLACEMENT_3D('',#23376,#19194,#19195);
#15662=AXIS2_PLACEMENT_3D('',#23377,#19196,#19197);
#15663=AXIS2_PLACEMENT_3D('',#23378,#19198,#19199);
#19180=DIRECTION('axis',(0.,0.,1.));
#19181=DIRECTION('refdir',(1.,0.,0.));
#19182=DIRECTION('center_axis',(0.,1.,0.));
#19183=DIRECTION('ref_axis',(1.,0.,0.));
#19184=DIRECTION('center_axis',(0.,-1.,0.));
#19185=DIRECTION('ref_axis',(1.,0.,0.));
#19186=DIRECTION('',(0.,-1.,0.));
#19187=DIRECTION('center_axis',(0.,-1.,0.));
#19188=DIRECTION('ref_axis',(1.,0.,0.));
#19189=DIRECTION('center_axis',(0.,1.,0.));
#19190=DIRECTION('ref_axis',(1.,0.,0.));
#19191=DIRECTION('center_axis',(0.,1.,0.));
#19192=DIRECTION('ref_axis',(1.,0.,0.));
#19193=DIRECTION('',(0.,-1.,0.));
#19194=DIRECTION('center_axis',(0.,1.,0.));
#19195=DIRECTION('ref_axis',(1.,0.,0.));
#19196=DIRECTION('center_axis',(0.,1.,0.));
#19197=DIRECTION('ref_axis',(1.,0.,0.));
#19198=DIRECTION('center_axis',(0.,1.,0.));
#19199=DIRECTION('ref_axis',(1.,0.,0.));
#23364=CARTESIAN_POINT('',(0.,0.,0.));
#23365=CARTESIAN_POINT('Origin',(19.3649167310371,6.,8.));
#23366=CARTESIAN_POINT('',(18.7599167310371,7.,8.));
#23367=CARTESIAN_POINT('Origin',(19.3649167310371,7.,8.));
#23368=CARTESIAN_POINT('',(18.7599167310371,6.,8.));
#23369=CARTESIAN_POINT('',(18.7599167310371,6.,8.));
#23370=CARTESIAN_POINT('Origin',(19.3649167310371,6.,8.));
#23371=CARTESIAN_POINT('Origin',(19.3649167310371,6.,8.));
#23372=CARTESIAN_POINT('',(18.5649167310371,7.,8.));
#23373=CARTESIAN_POINT('Origin',(19.3649167310371,7.,8.));
#23374=CARTESIAN_POINT('',(18.5649167310371,6.,8.));
#23375=CARTESIAN_POINT('',(18.5649167310371,6.,8.));
#23376=CARTESIAN_POINT('Origin',(19.3649167310371,6.,8.));
#23377=CARTESIAN_POINT('Origin',(19.3649167310371,7.,8.));
#23378=CARTESIAN_POINT('Origin',(19.3649167310371,6.,8.));
#24936=UNCERTAINTY_MEASURE_WITH_UNIT(LENGTH_MEASURE(0.001),#25101,
'DISTANCE_ACCURACY_VALUE',
'Maximum model space distance between geometric entities at asserted c
onnectivities');
#24979=UNCERTAINTY_MEASURE_WITH_UNIT(LENGTH_MEASURE(0.001),#25101,
'DISTANCE_ACCURACY_VALUE',
'Maximum model space distance between geometric entities at asserted c
onnectivities');
#25057=(
GEOMETRIC_REPRESENTATION_CONTEXT(3)
GLOBAL_UNCERTAINTY_ASSIGNED_CONTEXT((#24936))
GLOBAL_UNIT_ASSIGNED_CONTEXT((#25101,#25103,#25104))
REPRESENTATION_CONTEXT('','3D')
);
#25100=(
GEOMETRIC_REPRESENTATION_CONTEXT(3)
GLOBAL_UNCERTAINTY_ASSIGNED_CONTEXT((#24979))
GLOBAL_UNIT_ASSIGNED_CONTEXT((#25101,#25103,#25104))
REPRESENTATION_CONTEXT('','3D')
);
#25101=(
LENGTH_UNIT()
NAMED_UNIT(*)
SI_UNIT(.CENTI.,.METRE.)
);
#25103=(
NAMED_UNIT(*)
PLANE_ANGLE_UNIT()
SI_UNIT($,.RADIAN.)
);
#25104=(
NAMED_UNIT(*)
SI_UNIT($,.STERADIAN.)
SOLID_ANGLE_UNIT()
);
#25182=SHAPE_DEFINITION_REPRESENTATION(#25304,#25587);
#25304=PRODUCT_DEFINITION_SHAPE('',$,#25708);
#25587=SHAPE_REPRESENTATION('',(#15655),#25057);
#25630=PRODUCT_DEFINITION_CONTEXT('part definition',#25992,'design');
#25708=PRODUCT_DEFINITION('Axle distance sleeve 10 mm (2)',
'Axle distance sleeve 10 mm (2)',#25828,#25630);
#25828=PRODUCT_DEFINITION_FORMATION('',$,#26071);
#25992=APPLICATION_CONTEXT(
'Core Data for Automotive Mechanical Design Process');
#25993=PRODUCT_CONTEXT('part definition',#25992,'mechanical');
#26071=PRODUCT('Axle distance sleeve 10 mm (2)',
'Axle distance sleeve 10 mm (2)','Axle distance sleeve 10 mm (2)',(#25993));
#26185=COLOUR_RGB('Grey',0.48,0.52,0.57);
#26186=FILL_AREA_STYLE_COLOUR('',#26185);
#26187=FILL_AREA_STYLE('',(#26186));
#26188=SURFACE_STYLE_FILL_AREA(#26187);
#26189=SURFACE_SIDE_STYLE('',(#26188));
#26190=SURFACE_STYLE_USAGE(.BOTH.,#26189);
#26191=PRESENTATION_STYLE_ASSIGNMENT((#26190));
ENDSEC;
END-ISO-10303-21;
